ISO-10303-21;
HEADER;
FILE_DESCRIPTION (('STEP AP214'),
    '1' );
FILE_NAME ('socket head cap screw_iso_ISO 4762 M6 x 20 - 20N.step',
    '2026-10-08T09:53:37',
    ( '' ),
    ( '' ),
    'SwSTEP 2.0',
    'SolidWorks 2026',
    '' );
FILE_SCHEMA (( 'AUTOMOTIVE_DESIGN' ));
ENDSEC;

DATA;
#102=CARTESIAN_POINT ( 'NONE',  ( 26.00000000000000355, 0.000000000000000000, 0.000000000000000000 ) ) ;
#241=( NAMED_UNIT ( * ) PLANE_ANGLE_UNIT ( ) SI_UNIT ( $, .RADIAN. ) );
#370=VERTEX_POINT ( 'NONE', #32762 ) ;
#403=EDGE_CURVE ( 'NONE', #28480, #14622, #20753, .T. ) ;
#787=DIRECTION ( 'NONE',  ( -1.000000000000000000, -0.000000000000000000, -0.000000000000000000 ) ) ;
#901=ORIENTED_EDGE ( 'NONE', *, *, #23587, .F. ) ;
#1067=CARTESIAN_POINT ( 'NONE',  ( 3.000000000000000000, 0.000000000000000000, 0.000000000000000000 ) ) ;
#1208=DIRECTION ( 'NONE',  ( 0.000000000000000000, 0.000000000000000000, 1.000000000000000000 ) ) ;
#1209=PLANE ( 'NONE',  #42259 ) ;
#1386=VERTEX_POINT ( 'NONE', #54421 ) ;
#1573=DIRECTION ( 'NONE',  ( -0.000000000000000000, 1.625241993126352200E-15, 1.000000000000000000 ) ) ;
#1639=EDGE_LOOP ( 'NONE', ( #49549, #69239, #69076, #41140, #52089 ) ) ;
#1677=AXIS2_PLACEMENT_3D ( 'NONE', #55257, #34087, #27709 ) ;
#1732=DIRECTION ( 'NONE',  ( 1.000000000000000000, 0.000000000000000000, 0.000000000000000000 ) ) ;
#1782=AXIS2_PLACEMENT_3D ( 'NONE', #18093, #41035, #58311 ) ;
#1856=TOROIDAL_SURFACE ( 'NONE', #35462, 3.250000000000001332, 0.2500000000000000000 ) ;
#1952=CARTESIAN_POINT ( 'NONE',  ( -31.74999999999995737, 0.000000000000000000, 5.000000000000000000 ) ) ;
#1963=EDGE_CURVE ( 'NONE', #16556, #59396, #47406, .T. ) ;
#1981=DIRECTION ( 'NONE',  ( 0.000000000000000000, 0.000000000000000000, -1.000000000000000000 ) ) ;
#2485=VERTEX_POINT ( 'NONE', #52957 ) ;
#2529=EDGE_CURVE ( 'NONE', #54682, #42030, #66082, .T. ) ;
#2582=AXIS2_PLACEMENT_3D ( 'NONE', #25840, #48403, #66447 ) ;
#2658=FACE_OUTER_BOUND ( 'NONE', #6933, .T. ) ;
#2837=CARTESIAN_POINT ( 'NONE',  ( 3.000000000000000000, 2.935248768560057897, -3.252606517456513302E-15 ) ) ;
#2962=AXIS2_PLACEMENT_3D ( 'NONE', #17997, #33808, #63879 ) ;
#2973=VERTEX_POINT ( 'NONE', #62741 ) ;
#2999=ORIENTED_EDGE ( 'NONE', *, *, #6438, .F. ) ;
#3101=EDGE_CURVE ( 'NONE', #39686, #2973, #6963, .T. ) ;
#3150=EDGE_CURVE ( 'NONE', #32694, #28480, #57410, .T. ) ;
#3289=DIRECTION ( 'NONE',  ( -1.000000000000000000, -0.000000000000000000, -0.000000000000000000 ) ) ;
#3294=ORIENTED_EDGE ( 'NONE', *, *, #52699, .F. ) ;
#3395=AXIS2_PLACEMENT_3D ( 'NONE', #30919, #53862, #18898 ) ;
#3595=DIRECTION ( 'NONE',  ( -1.000000000000000000, 0.000000000000000000, -0.000000000000000000 ) ) ;
#3634=( NAMED_UNIT ( * ) PLANE_ANGLE_UNIT ( ) SI_UNIT ( $, .RADIAN. ) );
#3688=DIRECTION ( 'NONE',  ( 0.000000000000000000, 0.5000000000000009992, 0.8660254037844380415 ) ) ;
#3883=ORIENTED_EDGE ( 'NONE', *, *, #7508, .F. ) ;
#3921=EDGE_CURVE ( 'NONE', #19207, #32694, #61362, .T. ) ;
#3955=EDGE_CURVE ( 'NONE', #73325, #19590, #61054, .T. ) ;
#3999=( NAMED_UNIT ( * ) PLANE_ANGLE_UNIT ( ) SI_UNIT ( $, .RADIAN. ) );
#4063=AXIS2_PLACEMENT_3D ( 'NONE', #33719, #56671, #28071 ) ;
#4194=EDGE_LOOP ( 'NONE', ( #24713, #15446, #61971 ) ) ;
#4213=DIRECTION ( 'NONE',  ( 0.000000000000000000, -0.5000000000000012212, -0.8660254037844380415 ) ) ;
#4419=DIRECTION ( 'NONE',  ( -1.000000000000000000, -0.000000000000000000, -0.000000000000000000 ) ) ;
#4441=EDGE_CURVE ( 'NONE', #38665, #42030, #30216, .T. ) ;
#4585=CARTESIAN_POINT ( 'NONE',  ( 0.000000000000000000, 5.939536975864662969E-16, -4.700000000000000178 ) ) ;
#4863=ORIENTED_EDGE ( 'NONE', *, *, #62424, .F. ) ;
#4877=CARTESIAN_POINT ( 'NONE',  ( 0.000000000000000000, 1.467624384280025174, -2.542000000000001592 ) ) ;
#5020=ADVANCED_FACE ( 'NONE', ( #66710 ), #71588, .T. ) ;
#5445=EDGE_CURVE ( 'NONE', #59396, #38665, #25943, .T. ) ;
#5459=ORIENTED_EDGE ( 'NONE', *, *, #38976, .F. ) ;
#5641=DIRECTION ( 'NONE',  ( 0.000000000000000000, -0.5000000000000011102, -0.8660254037844380415 ) ) ;
#5729=VECTOR ( 'NONE', #45834, 1000.000000000000000 ) ;
#5753=VECTOR ( 'NONE', #28626, 999.9999999999998863 ) ;
#5811=AXIS2_PLACEMENT_3D ( 'NONE', #35728, #70303, #42138 ) ;
#5870=DIRECTION ( 'NONE',  ( -1.000000000000000000, -0.000000000000000000, -0.000000000000000000 ) ) ;
#6021=VECTOR ( 'NONE', #9682, 1000.000000000000114 ) ;
#6096=CARTESIAN_POINT ( 'NONE',  ( 0.000000000000000000, 2.935248768560057897, -3.252606517456513302E-15 ) ) ;
#6317=EDGE_CURVE ( 'NONE', #73325, #19207, #52564, .T. ) ;
#6324=DIRECTION ( 'NONE',  ( 0.000000000000000000, 0.000000000000000000, 1.000000000000000000 ) ) ;
#6376=AXIS2_PLACEMENT_3D ( 'NONE', #58575, #41650, #64591 ) ;
#6438=EDGE_CURVE ( 'NONE', #1386, #19207, #68080, .T. ) ;
#6481=ORIENTED_EDGE ( 'NONE', *, *, #1963, .T. ) ;
#6530=ORIENTED_EDGE ( 'NONE', *, *, #49987, .F. ) ;
#6842=DIRECTION ( 'NONE',  ( 1.000000000000000000, 0.000000000000000000, 0.000000000000000000 ) ) ;
#6933=EDGE_LOOP ( 'NONE', ( #44905, #10621, #14116, #51379, #39222 ) ) ;
#6963=CIRCLE ( 'NONE', #65787, 2.541999999999999815 ) ;
#6985=( GEOMETRIC_REPRESENTATION_CONTEXT ( 3 ) GLOBAL_UNCERTAINTY_ASSIGNED_CONTEXT ( ( #42869 ) ) GLOBAL_UNIT_ASSIGNED_CONTEXT ( ( #15634, #241, #11822 ) ) REPRESENTATION_CONTEXT ( 'NONE', 'WORKASPACE' ) );
#7069=CARTESIAN_POINT ( 'NONE',  ( 0.000000000000000000, 2.935248768560057897, -3.252606517456513302E-15 ) ) ;
#7080=AXIS2_PLACEMENT_3D ( 'NONE', #27236, #14487, #67481 ) ;
#7189=CARTESIAN_POINT ( 'NONE',  ( 6.250000000000005329, 3.673940397442060854E-16, -3.000000000000000888 ) ) ;
#7289=VECTOR ( 'NONE', #46261, 1000.000000000000000 ) ;
#7395=CARTESIAN_POINT ( 'NONE',  ( 0.000000000000000000, 0.000000000000000000, 4.700000000000000178 ) ) ;
#7508=EDGE_CURVE ( 'NONE', #18650, #39686, #36363, .T. ) ;
#7585=PLANE ( 'NONE',  #28630 ) ;
#7740=AXIS2_PLACEMENT_3D ( 'NONE', #22105, #38659, #67598 ) ;
#7816=DIRECTION ( 'NONE',  ( 0.000000000000000000, 0.000000000000000000, 1.000000000000000000 ) ) ;
#7889=PLANE ( 'NONE',  #33224 ) ;
#8176=CARTESIAN_POINT ( 'NONE',  ( -31.74999999999995737, 3.673940397442060854E-16, -3.000000000000000888 ) ) ;
#8206=MECHANICAL_DESIGN_GEOMETRIC_PRESENTATION_REPRESENTATION('',(#28606),#6985);
#8474=UNCERTAINTY_MEASURE_WITH_UNIT (LENGTH_MEASURE( 1.000000000000000082E-05 ), #32161, 'distance_accuracy_value', 'NONE');
#8598=ORIENTED_EDGE ( 'NONE', *, *, #3150, .T. ) ;
#8877=AXIS2_PLACEMENT_3D ( 'NONE', #65619, #3595, #70866 ) ;
#8934=VECTOR ( 'NONE', #22624, 1000.000000000000000 ) ;
#8939=CARTESIAN_POINT ( 'NONE',  ( 3.000000000000000000, 1.467624384280025174, -2.542000000000001592 ) ) ;
#8957=CARTESIAN_POINT ( 'NONE',  ( 0.000000000000000000, 2.935248768560057897, -3.252606517456513302E-15 ) ) ;
#9201=FACE_BOUND ( 'NONE', #37817, .T. ) ;
#9228=CARTESIAN_POINT ( 'NONE',  ( 3.000000000000000000, -1.467624384280027838, 2.542000000000001592 ) ) ;
#9265=FACE_OUTER_BOUND ( 'NONE', #67603, .T. ) ;
#9295=FACE_OUTER_BOUND ( 'NONE', #35570, .T. ) ;
#9551=DIRECTION ( 'NONE',  ( -1.000000000000000000, -0.000000000000000000, -0.000000000000000000 ) ) ;
#9682=DIRECTION ( 'NONE',  ( 0.000000000000000000, 0.4999999999999995004, -0.8660254037844389297 ) ) ;
#9774=VECTOR ( 'NONE', #9551, 1000.000000000000000 ) ;
#9778=CONICAL_SURFACE ( 'NONE', #59165, 2.445500000000000007, 0.7853981633974678189 ) ;
#9844=CARTESIAN_POINT ( 'NONE',  ( 3.000000000000000000, -1.467624384280032501, -2.541999999999998039 ) ) ;
#9900=CARTESIAN_POINT ( 'NONE',  ( 6.000000000000003553, 3.980102097228899218E-16, 3.250000000000001332 ) ) ;
#9981=FILL_AREA_STYLE_COLOUR ( '', #35794 ) ;
#10083=VECTOR ( 'NONE', #23615, 1000.000000000000114 ) ;
#10160=EDGE_LOOP ( 'NONE', ( #60662, #45532, #70859, #24155 ) ) ;
#10213=CARTESIAN_POINT ( 'NONE',  ( 3.000000000000000000, 2.935248768560057897, -3.252606517456513302E-15 ) ) ;
#10261=CARTESIAN_POINT ( 'NONE',  ( 5.999999999999998224, 6.123233995736766282E-16, -5.000000000000000000 ) ) ;
#10288=CYLINDRICAL_SURFACE ( 'NONE', #71537, 5.000000000000000000 ) ;
#10589=EDGE_CURVE ( 'NONE', #67486, #60096, #21005, .T. ) ;
#10621=ORIENTED_EDGE ( 'NONE', *, *, #33242, .F. ) ;
#10650=ORIENTED_EDGE ( 'NONE', *, *, #65218, .T. ) ;
#11019=VECTOR ( 'NONE', #15479, 1000.000000000000000 ) ;
#11038=CARTESIAN_POINT ( 'NONE',  ( -31.74999999999995737, 0.000000000000000000, 0.000000000000000000 ) ) ;
#11061=DIRECTION ( 'NONE',  ( 1.000000000000000000, 0.000000000000000000, 0.000000000000000000 ) ) ;
#11109=EDGE_CURVE ( 'NONE', #47680, #34322, #20176, .T. ) ;
#11191=DIRECTION ( 'NONE',  ( -0.7071067811865336949, 0.000000000000000000, 0.7071067811865613395 ) ) ;
#11447=CIRCLE ( 'NONE', #52234, 5.000000000000000000 ) ;
#11632=EDGE_LOOP ( 'NONE', ( #73612, #69824, #60299 ) ) ;
#11701=VECTOR ( 'NONE', #74002, 1000.000000000000114 ) ;
#11789=ORIENTED_EDGE ( 'NONE', *, *, #58297, .T. ) ;
#11822=( NAMED_UNIT ( * ) SI_UNIT ( $, .STERADIAN. ) SOLID_ANGLE_UNIT ( ) );
#12002=ORIENTED_EDGE ( 'NONE', *, *, #62602, .T. ) ;
#12020=CARTESIAN_POINT ( 'NONE',  ( 5.999999999999998224, 0.000000000000000000, 0.000000000000000000 ) ) ;
#12129=EDGE_CURVE ( 'NONE', #39032, #60096, #24731, .T. ) ;
#12291=LINE ( 'NONE', #46893, #32196 ) ;
#12311=CARTESIAN_POINT ( 'NONE',  ( 3.000000000000000000, 0.000000000000000000, 0.000000000000000000 ) ) ;
#12352=DIRECTION ( 'NONE',  ( 0.000000000000000000, -1.224646799147353207E-16, 1.000000000000000000 ) ) ;
#12460=VECTOR ( 'NONE', #34743, 1000.000000000000114 ) ;
#12597=CARTESIAN_POINT ( 'NONE',  ( 0.000000000000000000, 1.467624384280029837, 2.541999999999997151 ) ) ;
#12705=FACE_OUTER_BOUND ( 'NONE', #71743, .T. ) ;
#12950=ORIENTED_EDGE ( 'NONE', *, *, #66392, .F. ) ;
#13274=AXIS2_PLACEMENT_3D ( 'NONE', #40522, #46171, #58935 ) ;
#13413=CARTESIAN_POINT ( 'NONE',  ( 0.3000000000000016542, 6.123233995736766282E-16, -5.000000000000000000 ) ) ;
#13462=DIRECTION ( 'NONE',  ( -0.000000000000000000, 1.000000000000000000, 1.224646799147353207E-16 ) ) ;
#13531=( GEOMETRIC_REPRESENTATION_CONTEXT ( 3 ) GLOBAL_UNCERTAINTY_ASSIGNED_CONTEXT ( ( #8474 ) ) GLOBAL_UNIT_ASSIGNED_CONTEXT ( ( #32161, #3634, #59647 ) ) REPRESENTATION_CONTEXT ( 'NONE', 'WORKASPACE' ) );
#13626=FACE_OUTER_BOUND ( 'NONE', #10160, .T. ) ;
#13751=VECTOR ( 'NONE', #55337, 999.9999999999998863 ) ;
#13900=DIRECTION ( 'NONE',  ( 0.000000000000000000, 0.000000000000000000, -1.000000000000000000 ) ) ;
#13966=EDGE_LOOP ( 'NONE', ( #58338, #10650, #54833 ) ) ;
#14116=ORIENTED_EDGE ( 'NONE', *, *, #52036, .T. ) ;
#14187=CARTESIAN_POINT ( 'NONE',  ( 3.000000000000000000, 0.000000000000000000, 0.000000000000000000 ) ) ;
#14328=CARTESIAN_POINT ( 'NONE',  ( 3.000000000000000000, 2.935248768560057897, -3.252606517456513302E-15 ) ) ;
#14333=ORIENTED_EDGE ( 'NONE', *, *, #62045, .T. ) ;
#14487=DIRECTION ( 'NONE',  ( -1.000000000000000000, -0.000000000000000000, -0.000000000000000000 ) ) ;
#14561=DIRECTION ( 'NONE',  ( -1.000000000000000000, -0.000000000000000000, -0.000000000000000000 ) ) ;
#14569=DIRECTION ( 'NONE',  ( 0.000000000000000000, -1.181994176819165452E-15, -1.000000000000000000 ) ) ;
#14622=VERTEX_POINT ( 'NONE', #49200 ) ;
#14670=DIRECTION ( 'NONE',  ( 0.000000000000000000, -0.5000000000000011102, -0.8660254037844380415 ) ) ;
#14824=DIRECTION ( 'NONE',  ( 1.000000000000000000, 0.000000000000000000, 0.000000000000000000 ) ) ;
#14907=CARTESIAN_POINT ( 'NONE',  ( 25.44550000000002399, 3.673940397442060361E-16, -3.000000000000000444 ) ) ;
#15293=DIRECTION ( 'NONE',  ( -1.000000000000000000, -0.000000000000000000, -0.000000000000000000 ) ) ;
#15371=LINE ( 'NONE', #54496, #11701 ) ;
#15446=ORIENTED_EDGE ( 'NONE', *, *, #31555, .F. ) ;
#15479=DIRECTION ( 'NONE',  ( -1.000000000000000000, -0.000000000000000000, -0.000000000000000000 ) ) ;
#15482=VECTOR ( 'NONE', #15293, 1000.000000000000000 ) ;
#15634=( LENGTH_UNIT ( ) NAMED_UNIT ( * ) SI_UNIT ( .MILLI., .METRE. ) );
#15636=PRESENTATION_STYLE_ASSIGNMENT (( #50193 ) ) ;
#15685=CYLINDRICAL_SURFACE ( 'NONE', #59811, 3.000000000000000888 ) ;
#15809=EDGE_CURVE ( 'NONE', #19207, #67486, #49084, .T. ) ;
#15878=ORIENTED_EDGE ( 'NONE', *, *, #26134, .F. ) ;
#15897=EDGE_LOOP ( 'NONE', ( #31282, #39954, #35407, #48917 ) ) ;
#16011=CIRCLE ( 'NONE', #4063, 3.000000000000000888 ) ;
#16556=VERTEX_POINT ( 'NONE', #29656 ) ;
#16605=CIRCLE ( 'NONE', #20190, 3.000000000000000888 ) ;
#16744=CARTESIAN_POINT ( 'NONE',  ( 3.000000000000000000, -3.004629197474318063E-15, -2.541999999999999815 ) ) ;
#16750=SURFACE_STYLE_FILL_AREA ( #39688 ) ;
#16773=FACE_OUTER_BOUND ( 'NONE', #21696, .T. ) ;
#16974=CARTESIAN_POINT ( 'NONE',  ( 3.000000000000000000, -1.467624384280027838, 2.542000000000001592 ) ) ;
#17051=EDGE_CURVE ( 'NONE', #28480, #39686, #17351, .T. ) ;
#17156=CARTESIAN_POINT ( 'NONE',  ( 3.000000000000000000, 1.467624384280029837, 2.541999999999997151 ) ) ;
#17325=DIRECTION ( 'NONE',  ( -1.000000000000000000, -0.000000000000000000, -0.000000000000000000 ) ) ;
#17351=CIRCLE ( 'NONE', #59373, 2.541999999999999815 ) ;
#17657=LINE ( 'NONE', #35669, #17912 ) ;
#17665=EDGE_LOOP ( 'NONE', ( #66146, #73966 ) ) ;
#17689=VECTOR ( 'NONE', #48509, 1000.000000000000000 ) ;
#17812=CARTESIAN_POINT ( 'NONE',  ( 3.000000000000000000, 2.935248768560057897, -3.252606517456513302E-15 ) ) ;
#17912=VECTOR ( 'NONE', #28935, 1000.000000000000000 ) ;
#17997=CARTESIAN_POINT ( 'NONE',  ( 6.000000000000001776, 0.000000000000000000, 0.000000000000000000 ) ) ;
#18043=ORIENTED_EDGE ( 'NONE', *, *, #4441, .T. ) ;
#18093=CARTESIAN_POINT ( 'NONE',  ( 5.999999999999998224, 0.000000000000000000, 0.000000000000000000 ) ) ;
#18165=CARTESIAN_POINT ( 'NONE',  ( 0.3000000000000016542, 0.000000000000000000, 4.700000000000000178 ) ) ;
#18174=DIRECTION ( 'NONE',  ( -1.000000000000000000, -0.000000000000000000, -0.000000000000000000 ) ) ;
#18460=VERTEX_POINT ( 'NONE', #14907 ) ;
#18511=ADVANCED_FACE ( 'NONE', ( #9265 ), #52249, .F. ) ;
#18650=VERTEX_POINT ( 'NONE', #39332 ) ;
#18716=CYLINDRICAL_SURFACE ( 'NONE', #6376, 5.000000000000000000 ) ;
#18725=ADVANCED_FACE ( 'NONE', ( #16773 ), #1856, .F. ) ;
#18898=DIRECTION ( 'NONE',  ( 0.000000000000000000, 0.000000000000000000, 1.000000000000000000 ) ) ;
#19207=VERTEX_POINT ( 'NONE', #51248 ) ;
#19590=VERTEX_POINT ( 'NONE', #69878 ) ;
#19735=DIRECTION ( 'NONE',  ( 1.000000000000000000, 0.000000000000000000, 0.000000000000000000 ) ) ;
#19777=FILL_AREA_STYLE ('',( #48360 ) ) ;
#19874=VERTEX_POINT ( 'NONE', #9900 ) ;
#19934=LINE ( 'NONE', #47412, #52227 ) ;
#19950=CLOSED_SHELL ( 'NONE', ( #42893, #36755, #68081, #63577, #73857, #60437, #50519, #56280, #54351, #70120, #22173, #5020, #18725, #28532, #65307, #22440, #35457, #25376, #30889, #72228, #68185, #32933, #43433, #61318, #31044, #39748, #18511 ) ) ;
#19984=FACE_OUTER_BOUND ( 'NONE', #27276, .T. ) ;
#20176=LINE ( 'NONE', #43140, #66059 ) ;
#20190=AXIS2_PLACEMENT_3D ( 'NONE', #46660, #41033, #58310 ) ;
#20193=CYLINDRICAL_SURFACE ( 'NONE', #2582, 3.000000000000000888 ) ;
#20253=ORIENTED_EDGE ( 'NONE', *, *, #7508, .T. ) ;
#20289=AXIS2_PLACEMENT_3D ( 'NONE', #54221, #59861, #25635 ) ;
#20753=LINE ( 'NONE', #10213, #13751 ) ;
#21005=LINE ( 'NONE', #66873, #22747 ) ;
#21150=VECTOR ( 'NONE', #60174, 1000.000000000000114 ) ;
#21279=AXIS2_PLACEMENT_3D ( 'NONE', #30410, #53355, #24782 ) ;
#21410=ORIENTED_EDGE ( 'NONE', *, *, #72194, .T. ) ;
#21508=CONICAL_SURFACE ( 'NONE', #20289, 2.445500000000000007, 0.7853981633974678189 ) ;
#21535=ORIENTED_EDGE ( 'NONE', *, *, #28786, .T. ) ;
#21696=EDGE_LOOP ( 'NONE', ( #15878, #48183, #25469, #74244 ) ) ;
#22105=CARTESIAN_POINT ( 'NONE',  ( 3.000000000000000000, -2.935248768560059673, 2.602085213965210642E-15 ) ) ;
#22173=ADVANCED_FACE ( 'NONE', ( #13626 ), #9778, .T. ) ;
#22238=DIRECTION ( 'NONE',  ( -1.000000000000000000, -0.000000000000000000, -0.000000000000000000 ) ) ;
#22258=LINE ( 'NONE', #6096, #5753 ) ;
#22315=DIRECTION ( 'NONE',  ( 0.000000000000000000, 0.000000000000000000, 1.000000000000000000 ) ) ;
#22345=EDGE_CURVE ( 'NONE', #2485, #55377, #26754, .T. ) ;
#22385=( NAMED_UNIT ( * ) SI_UNIT ( $, .STERADIAN. ) SOLID_ANGLE_UNIT ( ) );
#22440=ADVANCED_FACE ( 'NONE', ( #41383 ), #1209, .F. ) ;
#22624=DIRECTION ( 'NONE',  ( -1.000000000000000000, -0.000000000000000000, -0.000000000000000000 ) ) ;
#22642=TOROIDAL_SURFACE ( 'NONE', #62263, 4.700000000000000178, 0.2999999999999999889 ) ;
#22747=VECTOR ( 'NONE', #72137, 1000.000000000000000 ) ;
#22754=ORIENTED_EDGE ( 'NONE', *, *, #3101, .T. ) ;
#22954=ORIENTED_EDGE ( 'NONE', *, *, #57322, .T. ) ;
#23332=CARTESIAN_POINT ( 'NONE',  ( 3.000000000000000000, 1.467624384280025174, -2.542000000000001592 ) ) ;
#23454=CARTESIAN_POINT ( 'NONE',  ( 0.000000000000000000, -2.935248768560059673, 2.602085213965210642E-15 ) ) ;
#23587=EDGE_CURVE ( 'NONE', #14622, #57906, #53157, .T. ) ;
#23615=DIRECTION ( 'NONE',  ( -0.5000000000000051070, 1.060575238724903217E-16, -0.8660254037844355990 ) ) ;
#24021=AXIS2_PLACEMENT_3D ( 'NONE', #59781, #25194, #36102 ) ;
#24155=ORIENTED_EDGE ( 'NONE', *, *, #60218, .F. ) ;
#24366=DIRECTION ( 'NONE',  ( 0.000000000000000000, -0.4999999999999998335, 0.8660254037844387076 ) ) ;
#24580=CARTESIAN_POINT ( 'NONE',  ( 3.000000000000000000, 1.467624384280025174, -2.542000000000001592 ) ) ;
#24704=ORIENTED_EDGE ( 'NONE', *, *, #5445, .T. ) ;
#24705=DIRECTION ( 'NONE',  ( 0.000000000000000000, 0.000000000000000000, 1.000000000000000000 ) ) ;
#24713=ORIENTED_EDGE ( 'NONE', *, *, #68586, .T. ) ;
#24731=LINE ( 'NONE', #7069, #65756 ) ;
#24782=DIRECTION ( 'NONE',  ( 0.000000000000000000, 0.000000000000000000, -1.000000000000000000 ) ) ;
#24959=CIRCLE ( 'NONE', #34564, 3.000000000000000444 ) ;
#25053=ORIENTED_EDGE ( 'NONE', *, *, #27830, .T. ) ;
#25060=DIRECTION ( 'NONE',  ( 0.000000000000000000, 0.000000000000000000, 1.000000000000000000 ) ) ;
#25063=ORIENTED_EDGE ( 'NONE', *, *, #403, .F. ) ;
#25113=PRODUCT_DEFINITION_CONTEXT ( 'detailed design', #43164, 'design' ) ;
#25176=DIRECTION ( 'NONE',  ( 0.000000000000000000, -0.8660254037844387076, -0.4999999999999998335 ) ) ;
#25187=DIRECTION ( 'NONE',  ( 0.000000000000000000, 0.000000000000000000, -1.000000000000000000 ) ) ;
#25194=DIRECTION ( 'NONE',  ( 0.000000000000000000, -1.000000000000000000, 0.000000000000000000 ) ) ;
#25367=FACE_OUTER_BOUND ( 'NONE', #11632, .T. ) ;
#25375=ORIENTED_EDGE ( 'NONE', *, *, #3955, .T. ) ;
#25376=ADVANCED_FACE ( 'NONE', ( #68351 ), #56848, .T. ) ;
#25469=ORIENTED_EDGE ( 'NONE', *, *, #71716, .T. ) ;
#25529=ORIENTED_EDGE ( 'NONE', *, *, #3955, .F. ) ;
#25546=ORIENTED_EDGE ( 'NONE', *, *, #4441, .F. ) ;
#25564=LINE ( 'NONE', #25931, #21150 ) ;
#25635=DIRECTION ( 'NONE',  ( 0.000000000000000000, 0.000000000000000000, 1.000000000000000000 ) ) ;
#25840=CARTESIAN_POINT ( 'NONE',  ( -31.74999999999995737, 0.000000000000000000, 0.000000000000000000 ) ) ;
#25931=CARTESIAN_POINT ( 'NONE',  ( 3.000000000000000000, -2.935248768560059673, 2.602085213965210642E-15 ) ) ;
#25943=CIRCLE ( 'NONE', #57199, 0.2999999999999999334 ) ;
#25965=DIRECTION ( 'NONE',  ( 0.000000000000000000, 0.000000000000000000, -1.000000000000000000 ) ) ;
#25997=ORIENTED_EDGE ( 'NONE', *, *, #51187, .T. ) ;
#26017=CARTESIAN_POINT ( 'NONE',  ( 3.000000000000000000, 2.201436576420041202, -1.271000000000003016 ) ) ;
#26134=EDGE_CURVE ( 'NONE', #34322, #19874, #72642, .T. ) ;
#26135=VECTOR ( 'NONE', #11191, 1000.000000000000000 ) ;
#26178=DIRECTION ( 'NONE',  ( 0.000000000000000000, 0.000000000000000000, 1.000000000000000000 ) ) ;
#26492=AXIS2_PLACEMENT_3D ( 'NONE', #36444, #25176, #43227 ) ;
#26754=LINE ( 'NONE', #9844, #11019 ) ;
#26886=LINE ( 'NONE', #49816, #42925 ) ;
#26969=ORIENTED_EDGE ( 'NONE', *, *, #33242, .T. ) ;
#26995=ORIENTED_EDGE ( 'NONE', *, *, #2529, .F. ) ;
#27236=CARTESIAN_POINT ( 'NONE',  ( 6.000000000000001776, 0.000000000000000000, 0.000000000000000000 ) ) ;
#27276=EDGE_LOOP ( 'NONE', ( #21535, #12002, #34405, #4863 ) ) ;
#27318=CARTESIAN_POINT ( 'NONE',  ( 3.000000000000000000, 2.935248768560057897, -3.252606517456513302E-15 ) ) ;
#27323=VECTOR ( 'NONE', #60881, 1000.000000000000114 ) ;
#27373=CARTESIAN_POINT ( 'NONE',  ( 3.000000000000000000, 0.000000000000000000, 0.000000000000000000 ) ) ;
#27527=VERTEX_POINT ( 'NONE', #47383 ) ;
#27657=CARTESIAN_POINT ( 'NONE',  ( 3.000000000000000000, 1.467624384280025174, -2.542000000000001592 ) ) ;
#27672=EDGE_CURVE ( 'NONE', #18650, #19207, #32288, .T. ) ;
#27709=DIRECTION ( 'NONE',  ( 0.000000000000000000, 0.000000000000000000, 1.000000000000000000 ) ) ;
#27830=EDGE_CURVE ( 'NONE', #19590, #69518, #15371, .T. ) ;
#27911=EDGE_CURVE ( 'NONE', #57906, #55377, #58470, .T. ) ;
#28010=ORIENTED_EDGE ( 'NONE', *, *, #27672, .F. ) ;
#28017=DIRECTION ( 'NONE',  ( 0.000000000000000000, -1.000000000000000000, 1.181994176819165452E-15 ) ) ;
#28071=DIRECTION ( 'NONE',  ( 0.000000000000000000, 0.000000000000000000, -1.000000000000000000 ) ) ;
#28085=LINE ( 'NONE', #55920, #46752 ) ;
#28402=CARTESIAN_POINT ( 'NONE',  ( 6.250000000000005329, 0.000000000000000000, 0.000000000000000000 ) ) ;
#28480=VERTEX_POINT ( 'NONE', #26017 ) ;
#28532=ADVANCED_FACE ( 'NONE', ( #32023 ), #73035, .T. ) ;
#28606=STYLED_ITEM ( 'NONE', ( #33271 ), #62892 ) ;
#28626=DIRECTION ( 'NONE',  ( 0.000000000000000000, -0.5000000000000012212, -0.8660254037844380415 ) ) ;
#28630=AXIS2_PLACEMENT_3D ( 'NONE', #14328, #6842, #1981 ) ;
#28706=CIRCLE ( 'NONE', #7080, 3.250000000000001332 ) ;
#28786=EDGE_CURVE ( 'NONE', #27527, #47885, #45493, .T. ) ;
#28933=AXIS2_PLACEMENT_3D ( 'NONE', #38861, #74178, #49756 ) ;
#28935=DIRECTION ( 'NONE',  ( -1.000000000000000000, -0.000000000000000000, -0.000000000000000000 ) ) ;
#29307=ORIENTED_EDGE ( 'NONE', *, *, #36414, .F. ) ;
#29344=DIRECTION ( 'NONE',  ( 0.000000000000000000, -1.000000000000000000, 1.625241993126352200E-15 ) ) ;
#29655=DIRECTION ( 'NONE',  ( -1.000000000000000000, -0.000000000000000000, -0.000000000000000000 ) ) ;
#29656=CARTESIAN_POINT ( 'NONE',  ( 5.999999999999998224, 0.000000000000000000, 5.000000000000000000 ) ) ;
#29729=DIRECTION ( 'NONE',  ( 0.000000000000000000, 0.4999999999999995004, -0.8660254037844389297 ) ) ;
#30065=DIRECTION ( 'NONE',  ( 0.000000000000000000, 0.000000000000000000, 1.000000000000000000 ) ) ;
#30128=ORIENTED_EDGE ( 'NONE', *, *, #11109, .F. ) ;
#30216=CIRCLE ( 'NONE', #30271, 4.700000000000000178 ) ;
#30271=AXIS2_PLACEMENT_3D ( 'NONE', #57185, #17325, #63205 ) ;
#30316=MECHANICAL_DESIGN_GEOMETRIC_PRESENTATION_REPRESENTATION('',(#57968),#42355);
#30352=ORIENTED_EDGE ( 'NONE', *, *, #65289, .T. ) ;
#30410=CARTESIAN_POINT ( 'NONE',  ( 6.000000000000001776, 5.000000000000000000, 0.000000000000000000 ) ) ;
#30491=PLANE ( 'NONE',  #38246 ) ;
#30805=CARTESIAN_POINT ( 'NONE',  ( 3.000000000000000000, 2.935248768560057897, -3.252606517456513302E-15 ) ) ;
#30828=FACE_OUTER_BOUND ( 'NONE', #74225, .T. ) ;
#30889=ADVANCED_FACE ( 'NONE', ( #37518 ), #66098, .F. ) ;
#30919=CARTESIAN_POINT ( 'NONE',  ( 3.000000000000000000, 0.000000000000000000, 0.000000000000000000 ) ) ;
#30975=DIRECTION ( 'NONE',  ( 0.000000000000000000, 1.000000000000000000, -1.224646799147353207E-16 ) ) ;
#31044=ADVANCED_FACE ( 'NONE', ( #25367 ), #65974, .F. ) ;
#31282=ORIENTED_EDGE ( 'NONE', *, *, #40194, .T. ) ;
#31445=EDGE_LOOP ( 'NONE', ( #71914, #49519 ) ) ;
#31555=EDGE_CURVE ( 'NONE', #2973, #2485, #57220, .T. ) ;
#31825=EDGE_CURVE ( 'NONE', #19590, #60096, #28085, .T. ) ;
#31967=FACE_OUTER_BOUND ( 'NONE', #43744, .T. ) ;
#32023=FACE_OUTER_BOUND ( 'NONE', #33371, .T. ) ;
#32120=FACE_OUTER_BOUND ( 'NONE', #40038, .T. ) ;
#32161=( LENGTH_UNIT ( ) NAMED_UNIT ( * ) SI_UNIT ( .MILLI., .METRE. ) );
#32196=VECTOR ( 'NONE', #69803, 1000.000000000000000 ) ;
#32288=LINE ( 'NONE', #61258, #27323 ) ;
#32320=DIRECTION ( 'NONE',  ( -1.000000000000000000, -0.000000000000000000, -0.000000000000000000 ) ) ;
#32430=CARTESIAN_POINT ( 'NONE',  ( 3.000000000000000000, 2.201436576420041202, 1.270999999999998575 ) ) ;
#32694=VERTEX_POINT ( 'NONE', #32430 ) ;
#32762=CARTESIAN_POINT ( 'NONE',  ( 3.000000000000000000, -2.935248768560059673, 2.602085213965210642E-15 ) ) ;
#32834=FACE_OUTER_BOUND ( 'NONE', #15897, .T. ) ;
#32933=ADVANCED_FACE ( 'NONE', ( #31967 ), #30491, .F. ) ;
#32958=CARTESIAN_POINT ( 'NONE',  ( -31.74999999999995737, 0.000000000000000000, 0.000000000000000000 ) ) ;
#32973=DIRECTION ( 'NONE',  ( 0.000000000000000000, 1.000000000000000000, -1.625241993126352398E-15 ) ) ;
#33057=CIRCLE ( 'NONE', #71486, 3.000000000000000444 ) ;
#33224=AXIS2_PLACEMENT_3D ( 'NONE', #30805, #53753, #25187 ) ;
#33242=EDGE_CURVE ( 'NONE', #70028, #39032, #17657, .T. ) ;
#33271=PRESENTATION_STYLE_ASSIGNMENT (( #61131 ) ) ;
#33342=AXIS2_PLACEMENT_3D ( 'NONE', #12311, #69457, #24705 ) ;
#33360=LINE ( 'NONE', #50662, #26135 ) ;
#33371=EDGE_LOOP ( 'NONE', ( #26995, #44384, #24704, #71663 ) ) ;
#33544=ORIENTED_EDGE ( 'NONE', *, *, #31825, .F. ) ;
#33659=( LENGTH_UNIT ( ) NAMED_UNIT ( * ) SI_UNIT ( .MILLI., .METRE. ) );
#33662=AXIS2_PLACEMENT_3D ( 'NONE', #27373, #50308, #44698 ) ;
#33719=CARTESIAN_POINT ( 'NONE',  ( 6.250000000000005329, 0.000000000000000000, 0.000000000000000000 ) ) ;
#33759=ORIENTED_EDGE ( 'NONE', *, *, #37035, .T. ) ;
#33808=DIRECTION ( 'NONE',  ( -1.000000000000000000, -0.000000000000000000, -0.000000000000000000 ) ) ;
#33814=PRODUCT_DEFINITION_SHAPE ( 'NONE', 'NONE',  #66939 ) ;
#33816=LINE ( 'NONE', #51106, #51480 ) ;
#34055=VECTOR ( 'NONE', #37135, 1000.000000000000000 ) ;
#34087=DIRECTION ( 'NONE',  ( 1.000000000000000000, 0.000000000000000000, 0.000000000000000000 ) ) ;
#34164=CIRCLE ( 'NONE', #1782, 5.000000000000000000 ) ;
#34173=DIRECTION ( 'NONE',  ( 0.000000000000000000, 1.000000000000000000, -1.625241993126352398E-15 ) ) ;
#34322=VERTEX_POINT ( 'NONE', #42917 ) ;
#34405=ORIENTED_EDGE ( 'NONE', *, *, #62045, .F. ) ;
#34564=AXIS2_PLACEMENT_3D ( 'NONE', #70247, #29655, #41331 ) ;
#34743=DIRECTION ( 'NONE',  ( 0.000000000000000000, -0.4999999999999998335, 0.8660254037844387076 ) ) ;
#35129=ORIENTED_EDGE ( 'NONE', *, *, #2529, .T. ) ;
#35243=EDGE_LOOP ( 'NONE', ( #33759, #22954 ) ) ;
#35407=ORIENTED_EDGE ( 'NONE', *, *, #51513, .T. ) ;
#35457=ADVANCED_FACE ( 'NONE', ( #9295 ), #55164, .T. ) ;
#35462=AXIS2_PLACEMENT_3D ( 'NONE', #28402, #51337, #68653 ) ;
#35570=EDGE_LOOP ( 'NONE', ( #57550, #25529, #51894, #40958, #25997 ) ) ;
#35634=CARTESIAN_POINT ( 'NONE',  ( 3.000000000000000000, -1.467624384280027838, 2.542000000000001592 ) ) ;
#35650=ORIENTED_EDGE ( 'NONE', *, *, #42180, .F. ) ;
#35669=CARTESIAN_POINT ( 'NONE',  ( 3.000000000000000000, 2.935248768560057897, -3.252606517456513302E-15 ) ) ;
#35728=CARTESIAN_POINT ( 'NONE',  ( 3.000000000000000000, 2.935248768560057897, -3.252606517456513302E-15 ) ) ;
#35794=COLOUR_RGB ( '', 0.09019608, 0.27058824, 0.51372549) ;
#36026=CARTESIAN_POINT ( 'NONE',  ( 0.3000000000000016542, 5.755839955992559655E-16, -4.700000000000000178 ) ) ;
#36102=DIRECTION ( 'NONE',  ( 0.000000000000000000, 0.000000000000000000, -1.000000000000000000 ) ) ;
#36363=LINE ( 'NONE', #59304, #10083 ) ;
#36414=EDGE_CURVE ( 'NONE', #39032, #57906, #22258, .T. ) ;
#36444=CARTESIAN_POINT ( 'NONE',  ( 3.000000000000000000, 2.935248768560057897, -3.252606517456513302E-15 ) ) ;
#36555=DIRECTION ( 'NONE',  ( 0.000000000000000000, 0.000000000000000000, 1.000000000000000000 ) ) ;
#36595=ORIENTED_EDGE ( 'NONE', *, *, #72194, .F. ) ;
#36635=AXIS2_PLACEMENT_3D ( 'NONE', #37484, #3289, #26178 ) ;
#36755=ADVANCED_FACE ( 'NONE', ( #48880 ), #22642, .T. ) ;
#36933=CARTESIAN_POINT ( 'NONE',  ( 3.000000000000000000, -1.467624384280027838, 2.542000000000001592 ) ) ;
#36966=CONICAL_SURFACE ( 'NONE', #3395, 2.541999999999999815, 1.047197551196591858 ) ;
#37035=EDGE_CURVE ( 'NONE', #60828, #19874, #28706, .T. ) ;
#37135=DIRECTION ( 'NONE',  ( -1.000000000000000000, -0.000000000000000000, -0.000000000000000000 ) ) ;
#37150=ORIENTED_EDGE ( 'NONE', *, *, #60218, .T. ) ;
#37484=CARTESIAN_POINT ( 'NONE',  ( 3.000000000000000000, 0.000000000000000000, 0.000000000000000000 ) ) ;
#37514=CARTESIAN_POINT ( 'NONE',  ( 3.000000000000000000, -1.467624384280027838, 2.542000000000001592 ) ) ;
#37518=FACE_OUTER_BOUND ( 'NONE', #73140, .T. ) ;
#37713=CARTESIAN_POINT ( 'NONE',  ( 0.000000000000000000, 1.467624384280025174, -2.542000000000001592 ) ) ;
#37817=EDGE_LOOP ( 'NONE', ( #71731, #33544, #25053, #64458, #52185, #29307 ) ) ;
#37937=PLANE ( 'NONE',  #26492 ) ;
#38117=DIRECTION ( 'NONE',  ( -1.000000000000000000, -0.000000000000000000, -0.000000000000000000 ) ) ;
#38246=AXIS2_PLACEMENT_3D ( 'NONE', #71816, #54909, #25965 ) ;
#38249=EDGE_LOOP ( 'NONE', ( #73167, #50799, #50969, #41603, #25375 ) ) ;
#38285=ORIENTED_EDGE ( 'NONE', *, *, #6317, .T. ) ;
#38659=DIRECTION ( 'NONE',  ( -0.000000000000000000, 0.8660254037844389297, 0.4999999999999995559 ) ) ;
#38665=VERTEX_POINT ( 'NONE', #7395 ) ;
#38861=CARTESIAN_POINT ( 'NONE',  ( 3.000000000000000000, 0.000000000000000000, 0.000000000000000000 ) ) ;
#38976=EDGE_CURVE ( 'NONE', #32694, #67486, #26886, .T. ) ;
#39032=VERTEX_POINT ( 'NONE', #8957 ) ;
#39151=CARTESIAN_POINT ( 'NONE',  ( 3.000000000000000000, 2.935248768560057897, -3.252606517456513302E-15 ) ) ;
#39217=ORIENTED_EDGE ( 'NONE', *, *, #26134, .T. ) ;
#39222=ORIENTED_EDGE ( 'NONE', *, *, #10589, .T. ) ;
#39239=CARTESIAN_POINT ( 'NONE',  ( 3.000000000000000000, -1.467624384280027838, 2.542000000000001592 ) ) ;
#39313=SURFACE_SIDE_STYLE ('',( #73876 ) ) ;
#39332=CARTESIAN_POINT ( 'NONE',  ( 4.467624384280048488, 0.000000000000000000, 0.000000000000000000 ) ) ;
#39474=AXIS2_PLACEMENT_3D ( 'NONE', #44061, #22238, #56078 ) ;
#39668=AXIS2_PLACEMENT_3D ( 'NONE', #36026, #13462, #12352 ) ;
#39686=VERTEX_POINT ( 'NONE', #16744 ) ;
#39688=FILL_AREA_STYLE ('',( #9981 ) ) ;
#39748=ADVANCED_FACE ( 'NONE', ( #65112 ), #7585, .F. ) ;
#39954=ORIENTED_EDGE ( 'NONE', *, *, #42180, .T. ) ;
#40038=EDGE_LOOP ( 'NONE', ( #18043, #30352 ) ) ;
#40194=EDGE_CURVE ( 'NONE', #16556, #54092, #53923, .T. ) ;
#40265=AXIS2_PLACEMENT_3D ( 'NONE', #59568, #30975, #54659 ) ;
#40522=CARTESIAN_POINT ( 'NONE',  ( 3.000000000000000000, 2.935248768560057897, -3.252606517456513302E-15 ) ) ;
#40757=AXIS2_PLACEMENT_3D ( 'NONE', #8939, #14569, #54796 ) ;
#40958=ORIENTED_EDGE ( 'NONE', *, *, #52699, .T. ) ;
#41000=CARTESIAN_POINT ( 'NONE',  ( 0.000000000000000000, 0.000000000000000000, 0.000000000000000000 ) ) ;
#41031=PLANE ( 'NONE',  #5811 ) ;
#41033=DIRECTION ( 'NONE',  ( 1.000000000000000000, 0.000000000000000000, 0.000000000000000000 ) ) ;
#41035=DIRECTION ( 'NONE',  ( -1.000000000000000000, -0.000000000000000000, -0.000000000000000000 ) ) ;
#41108=DIRECTION ( 'NONE',  ( 0.000000000000000000, -1.000000000000000000, 0.000000000000000000 ) ) ;
#41116=CARTESIAN_POINT ( 'NONE',  ( 6.250000000000005329, 0.000000000000000000, 0.000000000000000000 ) ) ;
#41140=ORIENTED_EDGE ( 'NONE', *, *, #31555, .T. ) ;
#41331=DIRECTION ( 'NONE',  ( 0.000000000000000000, 0.000000000000000000, 1.000000000000000000 ) ) ;
#41340=PLANE ( 'NONE',  #21279 ) ;
#41383=FACE_OUTER_BOUND ( 'NONE', #38249, .T. ) ;
#41603=ORIENTED_EDGE ( 'NONE', *, *, #6317, .F. ) ;
#41650=DIRECTION ( 'NONE',  ( -1.000000000000000000, -0.000000000000000000, -0.000000000000000000 ) ) ;
#41896=AXIS2_PLACEMENT_3D ( 'NONE', #12020, #787, #57530 ) ;
#42030=VERTEX_POINT ( 'NONE', #4585 ) ;
#42138=DIRECTION ( 'NONE',  ( 0.000000000000000000, 0.000000000000000000, -1.000000000000000000 ) ) ;
#42180=EDGE_CURVE ( 'NONE', #54092, #54682, #60802, .T. ) ;
#42259=AXIS2_PLACEMENT_3D ( 'NONE', #16974, #1573, #29344 ) ;
#42355=( GEOMETRIC_REPRESENTATION_CONTEXT ( 3 ) GLOBAL_UNCERTAINTY_ASSIGNED_CONTEXT ( ( #54336 ) ) GLOBAL_UNIT_ASSIGNED_CONTEXT ( ( #33659, #3999, #22385 ) ) REPRESENTATION_CONTEXT ( 'NONE', 'WORKASPACE' ) );
#42666=CARTESIAN_POINT ( 'NONE',  ( 26.00000000000000355, 2.445500000000000007, 0.000000000000000000 ) ) ;
#42869=UNCERTAINTY_MEASURE_WITH_UNIT (LENGTH_MEASURE( 1.000000000000000082E-05 ), #15634, 'distance_accuracy_value', 'NONE');
#42893=ADVANCED_FACE ( 'NONE', ( #58394 ), #36966, .F. ) ;
#42917=CARTESIAN_POINT ( 'NONE',  ( 6.250000000000005329, 0.000000000000000000, 3.000000000000000888 ) ) ;
#42925=VECTOR ( 'NONE', #61492, 1000.000000000000114 ) ;
#42982=EDGE_CURVE ( 'NONE', #47885, #27527, #46574, .T. ) ;
#43140=CARTESIAN_POINT ( 'NONE',  ( -31.74999999999995737, 0.000000000000000000, 3.000000000000000888 ) ) ;
#43155=LINE ( 'NONE', #8176, #34055 ) ;
#43164=APPLICATION_CONTEXT ( 'automotive_design' ) ;
#43227=DIRECTION ( 'NONE',  ( 0.000000000000000000, 0.4999999999999998335, -0.8660254037844387076 ) ) ;
#43395=AXIS2_PLACEMENT_3D ( 'NONE', #48320, #71232, #19735 ) ;
#43433=ADVANCED_FACE ( 'NONE', ( #30828 ), #41031, .F. ) ;
#43597=APPLICATION_CONTEXT ( 'automotive_design' ) ;
#43744=EDGE_LOOP ( 'NONE', ( #50487, #3294, #36595 ) ) ;
#43885=CARTESIAN_POINT ( 'NONE',  ( -31.74999999999995737, 6.123233995736766282E-16, -5.000000000000000000 ) ) ;
#43947=ORIENTED_EDGE ( 'NONE', *, *, #51254, .T. ) ;
#44061=CARTESIAN_POINT ( 'NONE',  ( 0.3000000000000016542, 0.000000000000000000, 0.000000000000000000 ) ) ;
#44260=FACE_OUTER_BOUND ( 'NONE', #54284, .T. ) ;
#44272=DIRECTION ( 'NONE',  ( 1.000000000000000000, 0.000000000000000000, 0.000000000000000000 ) ) ;
#44384=ORIENTED_EDGE ( 'NONE', *, *, #58297, .F. ) ;
#44513=ORIENTED_EDGE ( 'NONE', *, *, #15809, .T. ) ;
#44588=SHAPE_REPRESENTATION_RELATIONSHIP ( 'NONE' , 'NONE' ,  #50888, #52570 ) ;
#44698=DIRECTION ( 'NONE',  ( 0.000000000000000000, 0.000000000000000000, 1.000000000000000000 ) ) ;
#44734=EDGE_CURVE ( 'NONE', #69518, #55377, #55548, .T. ) ;
#44905=ORIENTED_EDGE ( 'NONE', *, *, #12129, .F. ) ;
#45493=CIRCLE ( 'NONE', #64693, 2.445500000000000007 ) ;
#45532=ORIENTED_EDGE ( 'NONE', *, *, #42982, .T. ) ;
#45834=DIRECTION ( 'NONE',  ( 0.000000000000000000, -1.000000000000000000, 1.181994176819165452E-15 ) ) ;
#46171=DIRECTION ( 'NONE',  ( 0.000000000000000000, 0.8660254037844379305, -0.5000000000000012212 ) ) ;
#46236=ORIENTED_EDGE ( 'NONE', *, *, #65218, .F. ) ;
#46261=DIRECTION ( 'NONE',  ( 0.000000000000000000, -1.000000000000000000, 1.181994176819165452E-15 ) ) ;
#46284=DIRECTION ( 'NONE',  ( -1.000000000000000000, -0.000000000000000000, -0.000000000000000000 ) ) ;
#46344=VECTOR ( 'NONE', #29729, 1000.000000000000114 ) ;
#46574=CIRCLE ( 'NONE', #66953, 2.445500000000000007 ) ;
#46660=CARTESIAN_POINT ( 'NONE',  ( 6.250000000000005329, 0.000000000000000000, 0.000000000000000000 ) ) ;
#46752=VECTOR ( 'NONE', #32973, 1000.000000000000000 ) ;
#46893=CARTESIAN_POINT ( 'NONE',  ( 26.00000000000000355, 2.994873747314852478E-16, -2.445500000000000007 ) ) ;
#46897=DIRECTION ( 'NONE',  ( -1.000000000000000000, -0.000000000000000000, -0.000000000000000000 ) ) ;
#46913=PLANE ( 'NONE',  #13274 ) ;
#47352=FACE_OUTER_BOUND ( 'NONE', #31445, .T. ) ;
#47383=CARTESIAN_POINT ( 'NONE',  ( 26.00000000000000355, 0.000000000000000000, 2.445500000000000007 ) ) ;
#47406=LINE ( 'NONE', #1952, #17689 ) ;
#47412=CARTESIAN_POINT ( 'NONE',  ( 3.000000000000000000, -1.467624384280027838, 2.542000000000001592 ) ) ;
#47680=VERTEX_POINT ( 'NONE', #54678 ) ;
#47885=VERTEX_POINT ( 'NONE', #73438 ) ;
#48102=CIRCLE ( 'NONE', #33662, 2.541999999999999815 ) ;
#48151=CARTESIAN_POINT ( 'NONE',  ( 0.3000000000000016542, 0.000000000000000000, 0.000000000000000000 ) ) ;
#48183=ORIENTED_EDGE ( 'NONE', *, *, #51590, .F. ) ;
#48204=CARTESIAN_POINT ( 'NONE',  ( 6.000000000000003553, 0.000000000000000000, -3.250000000000001332 ) ) ;
#48303=DIRECTION ( 'NONE',  ( 0.000000000000000000, 0.000000000000000000, -1.000000000000000000 ) ) ;
#48320=CARTESIAN_POINT ( 'NONE',  ( 0.000000000000000000, 0.000000000000000000, 0.000000000000000000 ) ) ;
#48360=FILL_AREA_STYLE_COLOUR ( '', #69929 ) ;
#48403=DIRECTION ( 'NONE',  ( -1.000000000000000000, -0.000000000000000000, -0.000000000000000000 ) ) ;
#48509=DIRECTION ( 'NONE',  ( -1.000000000000000000, -0.000000000000000000, -0.000000000000000000 ) ) ;
#48828=EDGE_LOOP ( 'NONE', ( #55080, #901, #25063, #12950, #26969 ) ) ;
#48880=FACE_OUTER_BOUND ( 'NONE', #56520, .T. ) ;
#48917=ORIENTED_EDGE ( 'NONE', *, *, #1963, .F. ) ;
#48984=ORIENTED_EDGE ( 'NONE', *, *, #51513, .F. ) ;
#49084=LINE ( 'NONE', #9228, #59220 ) ;
#49200=CARTESIAN_POINT ( 'NONE',  ( 3.000000000000000000, 1.467624384280025174, -2.542000000000001592 ) ) ;
#49299=ORIENTED_EDGE ( 'NONE', *, *, #3921, .F. ) ;
#49519=ORIENTED_EDGE ( 'NONE', *, *, #51254, .F. ) ;
#49549=ORIENTED_EDGE ( 'NONE', *, *, #44734, .F. ) ;
#49756=DIRECTION ( 'NONE',  ( 0.000000000000000000, 0.000000000000000000, 1.000000000000000000 ) ) ;
#49816=CARTESIAN_POINT ( 'NONE',  ( 3.000000000000000000, 2.935248768560057897, -3.252606517456513302E-15 ) ) ;
#49873=FACE_OUTER_BOUND ( 'NONE', #54464, .T. ) ;
#49987=EDGE_CURVE ( 'NONE', #18460, #70614, #43155, .T. ) ;
#50193=SURFACE_STYLE_USAGE ( .BOTH. , #39313 ) ;
#50266=DIRECTION ( 'NONE',  ( 0.000000000000000000, 0.000000000000000000, 1.000000000000000000 ) ) ;
#50308=DIRECTION ( 'NONE',  ( -1.000000000000000000, -0.000000000000000000, -0.000000000000000000 ) ) ;
#50487=ORIENTED_EDGE ( 'NONE', *, *, #68202, .F. ) ;
#50490=ORIENTED_EDGE ( 'NONE', *, *, #49987, .T. ) ;
#50519=ADVANCED_FACE ( 'NONE', ( #9201, #32120 ), #55062, .T. ) ;
#50662=CARTESIAN_POINT ( 'NONE',  ( 26.00000000000000355, 0.000000000000000000, 2.445500000000000007 ) ) ;
#50788=LINE ( 'NONE', #39151, #64390 ) ;
#50799=ORIENTED_EDGE ( 'NONE', *, *, #10589, .F. ) ;
#50888=SHAPE_REPRESENTATION ( 'socket head cap screw_iso_ISO 4762 M6 x 20 - 20N', ( #43395 ), #13531 ) ;
#50969=ORIENTED_EDGE ( 'NONE', *, *, #15809, .F. ) ;
#51106=CARTESIAN_POINT ( 'NONE',  ( 3.000000000000000000, -1.467624384280027838, 2.542000000000001592 ) ) ;
#51187=EDGE_CURVE ( 'NONE', #370, #69518, #64329, .T. ) ;
#51248=CARTESIAN_POINT ( 'NONE',  ( 3.000000000000000000, 4.131365146527187385E-15, 2.541999999999999371 ) ) ;
#51254=EDGE_CURVE ( 'NONE', #54092, #16556, #34164, .T. ) ;
#51337=DIRECTION ( 'NONE',  ( 1.000000000000000000, 0.000000000000000000, 0.000000000000000000 ) ) ;
#51379=ORIENTED_EDGE ( 'NONE', *, *, #38976, .T. ) ;
#51480=VECTOR ( 'NONE', #5641, 1000.000000000000114 ) ;
#51513=EDGE_CURVE ( 'NONE', #54682, #59396, #53256, .T. ) ;
#51560=CARTESIAN_POINT ( 'NONE',  ( 3.000000000000000000, -2.935248768560059673, 2.602085213965210642E-15 ) ) ;
#51590=EDGE_CURVE ( 'NONE', #70614, #34322, #16011, .T. ) ;
#51894=ORIENTED_EDGE ( 'NONE', *, *, #70852, .T. ) ;
#51995=DIRECTION ( 'NONE',  ( 0.000000000000000000, 0.000000000000000000, -1.000000000000000000 ) ) ;
#52036=EDGE_CURVE ( 'NONE', #70028, #32694, #64066, .T. ) ;
#52089=ORIENTED_EDGE ( 'NONE', *, *, #22345, .T. ) ;
#52185=ORIENTED_EDGE ( 'NONE', *, *, #27911, .F. ) ;
#52227=VECTOR ( 'NONE', #14670, 1000.000000000000114 ) ;
#52234=AXIS2_PLACEMENT_3D ( 'NONE', #61566, #44272, #50266 ) ;
#52249=CONICAL_SURFACE ( 'NONE', #36635, 2.541999999999999815, 1.047197551196591858 ) ;
#52310=CARTESIAN_POINT ( 'NONE',  ( 3.000000000000000000, -2.935248768560059673, 2.602085213965210642E-15 ) ) ;
#52321=EDGE_LOOP ( 'NONE', ( #69883, #39217, #53233, #72428 ) ) ;
#52564=LINE ( 'NONE', #35634, #59660 ) ;
#52570=ADVANCED_BREP_SHAPE_REPRESENTATION ( '', ( #62892, #43395 ), #13531 ) ;
#52699=EDGE_CURVE ( 'NONE', #1386, #370, #19934, .T. ) ;
#52831=DIRECTION ( 'NONE',  ( 0.000000000000000000, 0.000000000000000000, 1.000000000000000000 ) ) ;
#52957=CARTESIAN_POINT ( 'NONE',  ( 3.000000000000000000, -1.467624384280032501, -2.541999999999998039 ) ) ;
#52966=ORIENTED_EDGE ( 'NONE', *, *, #3921, .T. ) ;
#53157=LINE ( 'NONE', #24580, #65177 ) ;
#53233=ORIENTED_EDGE ( 'NONE', *, *, #37035, .F. ) ;
#53256=CIRCLE ( 'NONE', #1677, 5.000000000000000000 ) ;
#53355=DIRECTION ( 'NONE',  ( 1.000000000000000000, 0.000000000000000000, 0.000000000000000000 ) ) ;
#53529=TOROIDAL_SURFACE ( 'NONE', #63159, 3.250000000000001332, 0.2500000000000000000 ) ;
#53648=DIRECTION ( 'NONE',  ( -1.000000000000000000, -0.000000000000000000, -0.000000000000000000 ) ) ;
#53753=DIRECTION ( 'NONE',  ( 1.000000000000000000, 0.000000000000000000, 0.000000000000000000 ) ) ;
#53862=DIRECTION ( 'NONE',  ( -1.000000000000000000, -0.000000000000000000, -0.000000000000000000 ) ) ;
#53923=CIRCLE ( 'NONE', #41896, 5.000000000000000000 ) ;
#53990=EDGE_LOOP ( 'NONE', ( #44513, #5459, #49299 ) ) ;
#54092=VERTEX_POINT ( 'NONE', #10261 ) ;
#54140=AXIS2_PLACEMENT_3D ( 'NONE', #41000, #63931, #30065 ) ;
#54145=AXIS2_PLACEMENT_3D ( 'NONE', #37514, #54792, #3688 ) ;
#54221=CARTESIAN_POINT ( 'NONE',  ( 26.00000000000000355, 0.000000000000000000, 0.000000000000000000 ) ) ;
#54242=CARTESIAN_POINT ( 'NONE',  ( 26.00000000000000355, 0.000000000000000000, 0.000000000000000000 ) ) ;
#54284=EDGE_LOOP ( 'NONE', ( #6530, #37150, #54562, #64558 ) ) ;
#54336=UNCERTAINTY_MEASURE_WITH_UNIT (LENGTH_MEASURE( 1.000000000000000082E-05 ), #33659, 'distance_accuracy_value', 'NONE');
#54351=ADVANCED_FACE ( 'NONE', ( #59008, #47352 ), #41340, .T. ) ;
#54421=CARTESIAN_POINT ( 'NONE',  ( 3.000000000000000000, -2.201436576420043867, 1.271000000000003904 ) ) ;
#54464=EDGE_LOOP ( 'NONE', ( #14333, #50490, #60665, #30128 ) ) ;
#54496=CARTESIAN_POINT ( 'NONE',  ( 0.000000000000000000, -1.467624384280027838, 2.542000000000001592 ) ) ;
#54513=FACE_OUTER_BOUND ( 'NONE', #4194, .T. ) ;
#54562=ORIENTED_EDGE ( 'NONE', *, *, #11109, .T. ) ;
#54567=CARTESIAN_POINT ( 'NONE',  ( 0.3000000000000016542, 0.000000000000000000, 5.000000000000000000 ) ) ;
#54659=DIRECTION ( 'NONE',  ( 0.000000000000000000, 1.224646799147351482E-16, 1.000000000000000000 ) ) ;
#54678=CARTESIAN_POINT ( 'NONE',  ( 25.44550000000002399, 0.000000000000000000, 3.000000000000000444 ) ) ;
#54682=VERTEX_POINT ( 'NONE', #13413 ) ;
#54792=DIRECTION ( 'NONE',  ( 0.000000000000000000, 0.8660254037844380415, -0.5000000000000009992 ) ) ;
#54796=DIRECTION ( 'NONE',  ( 0.000000000000000000, 1.000000000000000000, -1.181994176819165452E-15 ) ) ;
#54801=CARTESIAN_POINT ( 'NONE',  ( 0.000000000000000000, -2.935248768560059673, 2.602085213965210642E-15 ) ) ;
#54811=AXIS2_PLACEMENT_3D ( 'NONE', #72161, #72524, #13900 ) ;
#54833=ORIENTED_EDGE ( 'NONE', *, *, #17051, .F. ) ;
#54875=AXIS2_PLACEMENT_3D ( 'NONE', #14187, #14561, #7816 ) ;
#54909=DIRECTION ( 'NONE',  ( 1.000000000000000000, 0.000000000000000000, 0.000000000000000000 ) ) ;
#55062=PLANE ( 'NONE',  #8877 ) ;
#55080=ORIENTED_EDGE ( 'NONE', *, *, #36414, .T. ) ;
#55164=PLANE ( 'NONE',  #54145 ) ;
#55257=CARTESIAN_POINT ( 'NONE',  ( 0.3000000000000016542, 0.000000000000000000, 0.000000000000000000 ) ) ;
#55266=DIRECTION ( 'NONE',  ( 0.000000000000000000, 0.000000000000000000, 1.000000000000000000 ) ) ;
#55337=DIRECTION ( 'NONE',  ( 0.000000000000000000, -0.5000000000000012212, -0.8660254037844380415 ) ) ;
#55377=VERTEX_POINT ( 'NONE', #70383 ) ;
#55548=LINE ( 'NONE', #54801, #6021 ) ;
#55673=ORIENTED_EDGE ( 'NONE', *, *, #23587, .T. ) ;
#55920=CARTESIAN_POINT ( 'NONE',  ( 0.000000000000000000, -1.467624384280027838, 2.542000000000001592 ) ) ;
#56078=DIRECTION ( 'NONE',  ( 0.000000000000000000, 0.000000000000000000, 1.000000000000000000 ) ) ;
#56137=PRODUCT_CONTEXT ( 'NONE', #43597, 'mechanical' ) ;
#56280=ADVANCED_FACE ( 'NONE', ( #12705 ), #18716, .T. ) ;
#56431=CIRCLE ( 'NONE', #24021, 0.2500000000000002220 ) ;
#56520=EDGE_LOOP ( 'NONE', ( #48984, #35129, #25546, #58850 ) ) ;
#56671=DIRECTION ( 'NONE',  ( 1.000000000000000000, 0.000000000000000000, 0.000000000000000000 ) ) ;
#56848=PLANE ( 'NONE',  #7740 ) ;
#57185=CARTESIAN_POINT ( 'NONE',  ( 0.000000000000000000, 0.000000000000000000, 0.000000000000000000 ) ) ;
#57199=AXIS2_PLACEMENT_3D ( 'NONE', #18165, #41108, #51995 ) ;
#57220=LINE ( 'NONE', #52310, #46344 ) ;
#57322=EDGE_CURVE ( 'NONE', #19874, #60828, #72555, .T. ) ;
#57345=LINE ( 'NONE', #27657, #70409 ) ;
#57410=CIRCLE ( 'NONE', #33342, 2.541999999999999815 ) ;
#57530=DIRECTION ( 'NONE',  ( 0.000000000000000000, 0.000000000000000000, 1.000000000000000000 ) ) ;
#57550=ORIENTED_EDGE ( 'NONE', *, *, #27830, .F. ) ;
#57906=VERTEX_POINT ( 'NONE', #37713 ) ;
#57968=STYLED_ITEM ( 'NONE', ( #15636 ), #52570 ) ;
#58027=FACE_OUTER_BOUND ( 'NONE', #52321, .T. ) ;
#58297=EDGE_CURVE ( 'NONE', #59396, #54682, #11447, .T. ) ;
#58310=DIRECTION ( 'NONE',  ( 0.000000000000000000, 0.000000000000000000, -1.000000000000000000 ) ) ;
#58311=DIRECTION ( 'NONE',  ( 0.000000000000000000, 0.000000000000000000, 1.000000000000000000 ) ) ;
#58338=ORIENTED_EDGE ( 'NONE', *, *, #403, .T. ) ;
#58394=FACE_OUTER_BOUND ( 'NONE', #59452, .T. ) ;
#58470=LINE ( 'NONE', #4877, #5729 ) ;
#58575=CARTESIAN_POINT ( 'NONE',  ( -31.74999999999995737, 0.000000000000000000, 0.000000000000000000 ) ) ;
#58850=ORIENTED_EDGE ( 'NONE', *, *, #5445, .F. ) ;
#58935=DIRECTION ( 'NONE',  ( 0.000000000000000000, 0.5000000000000012212, 0.8660254037844379305 ) ) ;
#59008=FACE_BOUND ( 'NONE', #35243, .T. ) ;
#59029=LINE ( 'NONE', #23332, #7289 ) ;
#59165=AXIS2_PLACEMENT_3D ( 'NONE', #54242, #65157, #36555 ) ;
#59206=DIRECTION ( 'NONE',  ( 0.000000000000000000, 0.000000000000000000, -1.000000000000000000 ) ) ;
#59220=VECTOR ( 'NONE', #71636, 1000.000000000000000 ) ;
#59304=CARTESIAN_POINT ( 'NONE',  ( 3.000000000000000000, 3.113052163432572109E-16, -2.541999999999999815 ) ) ;
#59373=AXIS2_PLACEMENT_3D ( 'NONE', #1067, #46897, #25060 ) ;
#59396=VERTEX_POINT ( 'NONE', #54567 ) ;
#59401=FACE_OUTER_BOUND ( 'NONE', #53990, .T. ) ;
#59452=EDGE_LOOP ( 'NONE', ( #28010, #20253, #22754, #21410, #60877 ) ) ;
#59568=CARTESIAN_POINT ( 'NONE',  ( 6.250000000000005329, 3.980102097228899218E-16, 3.250000000000001332 ) ) ;
#59647=( NAMED_UNIT ( * ) SI_UNIT ( $, .STERADIAN. ) SOLID_ANGLE_UNIT ( ) );
#59660=VECTOR ( 'NONE', #34173, 1000.000000000000000 ) ;
#59781=CARTESIAN_POINT ( 'NONE',  ( 6.250000000000005329, 0.000000000000000000, -3.250000000000001332 ) ) ;
#59811=AXIS2_PLACEMENT_3D ( 'NONE', #32958, #4419, #68310 ) ;
#59861=DIRECTION ( 'NONE',  ( -1.000000000000000000, -0.000000000000000000, -0.000000000000000000 ) ) ;
#60096=VERTEX_POINT ( 'NONE', #12597 ) ;
#60174=DIRECTION ( 'NONE',  ( 0.000000000000000000, 0.4999999999999995004, -0.8660254037844389297 ) ) ;
#60218=EDGE_CURVE ( 'NONE', #18460, #47680, #33057, .T. ) ;
#60299=ORIENTED_EDGE ( 'NONE', *, *, #3150, .F. ) ;
#60437=ADVANCED_FACE ( 'NONE', ( #32834 ), #10288, .T. ) ;
#60482=ORIENTED_EDGE ( 'NONE', *, *, #22345, .F. ) ;
#60662=ORIENTED_EDGE ( 'NONE', *, *, #62602, .F. ) ;
#60665=ORIENTED_EDGE ( 'NONE', *, *, #51590, .T. ) ;
#60802=LINE ( 'NONE', #43885, #15482 ) ;
#60828=VERTEX_POINT ( 'NONE', #48204 ) ;
#60877=ORIENTED_EDGE ( 'NONE', *, *, #6438, .T. ) ;
#60881=DIRECTION ( 'NONE',  ( -0.5000000000000051070, 0.000000000000000000, 0.8660254037844355990 ) ) ;
#61054=LINE ( 'NONE', #39239, #9774 ) ;
#61131=SURFACE_STYLE_USAGE ( .BOTH. , #62627 ) ;
#61258=CARTESIAN_POINT ( 'NONE',  ( 3.000000000000000000, 0.000000000000000000, 2.541999999999999815 ) ) ;
#61318=ADVANCED_FACE ( 'NONE', ( #59401 ), #7889, .F. ) ;
#61362=CIRCLE ( 'NONE', #28933, 2.541999999999999815 ) ;
#61417=SHAPE_DEFINITION_REPRESENTATION ( #33814, #50888 ) ;
#61492=DIRECTION ( 'NONE',  ( 0.000000000000000000, -0.4999999999999998335, 0.8660254037844387076 ) ) ;
#61566=CARTESIAN_POINT ( 'NONE',  ( 0.3000000000000016542, 0.000000000000000000, 0.000000000000000000 ) ) ;
#61971=ORIENTED_EDGE ( 'NONE', *, *, #3101, .F. ) ;
#62045=EDGE_CURVE ( 'NONE', #47680, #18460, #24959, .T. ) ;
#62263=AXIS2_PLACEMENT_3D ( 'NONE', #48151, #32320, #55266 ) ;
#62424=EDGE_CURVE ( 'NONE', #27527, #47680, #33360, .T. ) ;
#62524=CIRCLE ( 'NONE', #54140, 4.700000000000000178 ) ;
#62602=EDGE_CURVE ( 'NONE', #47885, #18460, #12291, .T. ) ;
#62627=SURFACE_SIDE_STYLE ('',( #16750 ) ) ;
#62741=CARTESIAN_POINT ( 'NONE',  ( 3.000000000000000000, -2.201436576420044755, -1.270999999999999019 ) ) ;
#62892=MANIFOLD_SOLID_BREP ( 'Hex', #19950 ) ;
#63159=AXIS2_PLACEMENT_3D ( 'NONE', #41116, #11061, #64052 ) ;
#63205=DIRECTION ( 'NONE',  ( 0.000000000000000000, 0.000000000000000000, 1.000000000000000000 ) ) ;
#63535=ORIENTED_EDGE ( 'NONE', *, *, #27911, .T. ) ;
#63577=ADVANCED_FACE ( 'NONE', ( #19984 ), #21508, .T. ) ;
#63751=CARTESIAN_POINT ( 'NONE',  ( 25.44550000000002399, 0.000000000000000000, 0.000000000000000000 ) ) ;
#63799=ORIENTED_EDGE ( 'NONE', *, *, #27672, .T. ) ;
#63879=DIRECTION ( 'NONE',  ( 0.000000000000000000, 0.000000000000000000, -1.000000000000000000 ) ) ;
#63931=DIRECTION ( 'NONE',  ( -1.000000000000000000, -0.000000000000000000, -0.000000000000000000 ) ) ;
#64052=DIRECTION ( 'NONE',  ( 0.000000000000000000, 0.000000000000000000, -1.000000000000000000 ) ) ;
#64053=DIRECTION ( 'NONE',  ( 0.000000000000000000, 0.000000000000000000, 1.000000000000000000 ) ) ;
#64066=LINE ( 'NONE', #17812, #12460 ) ;
#64329=LINE ( 'NONE', #51560, #8934 ) ;
#64390=VECTOR ( 'NONE', #4213, 999.9999999999998863 ) ;
#64458=ORIENTED_EDGE ( 'NONE', *, *, #44734, .T. ) ;
#64558=ORIENTED_EDGE ( 'NONE', *, *, #69953, .T. ) ;
#64591=DIRECTION ( 'NONE',  ( 0.000000000000000000, 0.000000000000000000, 1.000000000000000000 ) ) ;
#64693=AXIS2_PLACEMENT_3D ( 'NONE', #102, #46284, #1208 ) ;
#65112=FACE_OUTER_BOUND ( 'NONE', #13966, .T. ) ;
#65157=DIRECTION ( 'NONE',  ( -1.000000000000000000, -0.000000000000000000, -0.000000000000000000 ) ) ;
#65177=VECTOR ( 'NONE', #69703, 1000.000000000000000 ) ;
#65218=EDGE_CURVE ( 'NONE', #14622, #39686, #59029, .T. ) ;
#65289=EDGE_CURVE ( 'NONE', #42030, #38665, #62524, .T. ) ;
#65307=ADVANCED_FACE ( 'NONE', ( #2658 ), #37937, .T. ) ;
#65435=PLANE ( 'NONE',  #54811 ) ;
#65619=CARTESIAN_POINT ( 'NONE',  ( 0.000000000000000000, 0.000000000000000000, 0.000000000000000000 ) ) ;
#65756=VECTOR ( 'NONE', #24366, 1000.000000000000114 ) ;
#65787=AXIS2_PLACEMENT_3D ( 'NONE', #69102, #53648, #6324 ) ;
#65974=PLANE ( 'NONE',  #65992 ) ;
#65992=AXIS2_PLACEMENT_3D ( 'NONE', #2837, #1732, #59206 ) ;
#66059=VECTOR ( 'NONE', #72422, 1000.000000000000000 ) ;
#66082=CIRCLE ( 'NONE', #39668, 0.2999999999999999334 ) ;
#66098=PLANE ( 'NONE',  #40757 ) ;
#66146=ORIENTED_EDGE ( 'NONE', *, *, #28786, .F. ) ;
#66392=EDGE_CURVE ( 'NONE', #70028, #28480, #50788, .T. ) ;
#66447=DIRECTION ( 'NONE',  ( 0.000000000000000000, 0.000000000000000000, 1.000000000000000000 ) ) ;
#66710=FACE_OUTER_BOUND ( 'NONE', #17665, .T. ) ;
#66873=CARTESIAN_POINT ( 'NONE',  ( 3.000000000000000000, 1.467624384280029837, 2.541999999999997151 ) ) ;
#66939=PRODUCT_DEFINITION ( 'UNKNOWN', '', #71206, #25113 ) ;
#66953=AXIS2_PLACEMENT_3D ( 'NONE', #69677, #18174, #64053 ) ;
#67218=ORIENTED_EDGE ( 'NONE', *, *, #70852, .F. ) ;
#67481=DIRECTION ( 'NONE',  ( 0.000000000000000000, 0.000000000000000000, -1.000000000000000000 ) ) ;
#67486=VERTEX_POINT ( 'NONE', #17156 ) ;
#67598=DIRECTION ( 'NONE',  ( 0.000000000000000000, -0.4999999999999995559, 0.8660254037844389297 ) ) ;
#67603=EDGE_LOOP ( 'NONE', ( #3883, #63799, #52966, #8598, #70645 ) ) ;
#67876=ORIENTED_EDGE ( 'NONE', *, *, #68586, .F. ) ;
#68080=CIRCLE ( 'NONE', #54875, 2.541999999999999815 ) ;
#68081=ADVANCED_FACE ( 'NONE', ( #58027 ), #53529, .F. ) ;
#68185=ADVANCED_FACE ( 'NONE', ( #54513 ), #65435, .F. ) ;
#68202=EDGE_CURVE ( 'NONE', #370, #2973, #25564, .T. ) ;
#68310=DIRECTION ( 'NONE',  ( 0.000000000000000000, 0.000000000000000000, 1.000000000000000000 ) ) ;
#68351=FACE_OUTER_BOUND ( 'NONE', #1639, .T. ) ;
#68586=EDGE_CURVE ( 'NONE', #39686, #2485, #57345, .T. ) ;
#68653=DIRECTION ( 'NONE',  ( 0.000000000000000000, 0.000000000000000000, -1.000000000000000000 ) ) ;
#69076=ORIENTED_EDGE ( 'NONE', *, *, #68202, .T. ) ;
#69102=CARTESIAN_POINT ( 'NONE',  ( 3.000000000000000000, 0.000000000000000000, 0.000000000000000000 ) ) ;
#69239=ORIENTED_EDGE ( 'NONE', *, *, #51187, .F. ) ;
#69457=DIRECTION ( 'NONE',  ( -1.000000000000000000, -0.000000000000000000, -0.000000000000000000 ) ) ;
#69518=VERTEX_POINT ( 'NONE', #23454 ) ;
#69677=CARTESIAN_POINT ( 'NONE',  ( 26.00000000000000355, 0.000000000000000000, 0.000000000000000000 ) ) ;
#69703=DIRECTION ( 'NONE',  ( -1.000000000000000000, -0.000000000000000000, -0.000000000000000000 ) ) ;
#69803=DIRECTION ( 'NONE',  ( -0.7071067811865336949, 8.659560562355101724E-17, -0.7071067811865613395 ) ) ;
#69823=FACE_OUTER_BOUND ( 'NONE', #48828, .T. ) ;
#69824=ORIENTED_EDGE ( 'NONE', *, *, #66392, .T. ) ;
#69878=CARTESIAN_POINT ( 'NONE',  ( 0.000000000000000000, -1.467624384280027838, 2.542000000000001592 ) ) ;
#69883=ORIENTED_EDGE ( 'NONE', *, *, #69953, .F. ) ;
#69929=COLOUR_RGB ( '', 0.09019608, 0.27058824, 0.51372549) ;
#69953=EDGE_CURVE ( 'NONE', #34322, #70614, #16605, .T. ) ;
#70028=VERTEX_POINT ( 'NONE', #27318 ) ;
#70120=ADVANCED_FACE ( 'NONE', ( #44260 ), #15685, .T. ) ;
#70247=CARTESIAN_POINT ( 'NONE',  ( 25.44550000000002399, 0.000000000000000000, 0.000000000000000000 ) ) ;
#70303=DIRECTION ( 'NONE',  ( 1.000000000000000000, 0.000000000000000000, 0.000000000000000000 ) ) ;
#70311=AXIS2_PLACEMENT_3D ( 'NONE', #42666, #14824, #48303 ) ;
#70383=CARTESIAN_POINT ( 'NONE',  ( 0.000000000000000000, -1.467624384280032501, -2.541999999999998039 ) ) ;
#70409=VECTOR ( 'NONE', #28017, 1000.000000000000000 ) ;
#70614=VERTEX_POINT ( 'NONE', #7189 ) ;
#70645=ORIENTED_EDGE ( 'NONE', *, *, #17051, .T. ) ;
#70852=EDGE_CURVE ( 'NONE', #73325, #1386, #33816, .T. ) ;
#70859=ORIENTED_EDGE ( 'NONE', *, *, #62424, .T. ) ;
#70866=DIRECTION ( 'NONE',  ( -0.000000000000000000, 0.000000000000000000, 1.000000000000000000 ) ) ;
#71206=PRODUCT_DEFINITION_FORMATION_WITH_SPECIFIED_SOURCE ( 'ANY', '', #71551, .NOT_KNOWN. ) ;
#71232=DIRECTION ( 'NONE',  ( 0.000000000000000000, 0.000000000000000000, 1.000000000000000000 ) ) ;
#71486=AXIS2_PLACEMENT_3D ( 'NONE', #63751, #5870, #52831 ) ;
#71537=AXIS2_PLACEMENT_3D ( 'NONE', #11038, #38117, #22315 ) ;
#71551=PRODUCT ( 'socket head cap screw_iso_ISO 4762 M6 x 20 - 20N', 'socket head cap screw_iso_ISO 4762 M6 x 20 - 20N', '', ( #56137 ) ) ;
#71588=PLANE ( 'NONE',  #70311 ) ;
#71636=DIRECTION ( 'NONE',  ( 0.000000000000000000, 1.000000000000000000, -1.625241993126352398E-15 ) ) ;
#71663=ORIENTED_EDGE ( 'NONE', *, *, #65289, .F. ) ;
#71716=EDGE_CURVE ( 'NONE', #70614, #60828, #56431, .T. ) ;
#71731=ORIENTED_EDGE ( 'NONE', *, *, #12129, .T. ) ;
#71743=EDGE_LOOP ( 'NONE', ( #35650, #43947, #6481, #11789 ) ) ;
#71816=CARTESIAN_POINT ( 'NONE',  ( 3.000000000000000000, 2.935248768560057897, -3.252606517456513302E-15 ) ) ;
#71914=ORIENTED_EDGE ( 'NONE', *, *, #40194, .F. ) ;
#72137=DIRECTION ( 'NONE',  ( -1.000000000000000000, -0.000000000000000000, -0.000000000000000000 ) ) ;
#72161=CARTESIAN_POINT ( 'NONE',  ( 3.000000000000000000, 2.935248768560057897, -3.252606517456513302E-15 ) ) ;
#72194=EDGE_CURVE ( 'NONE', #2973, #1386, #48102, .T. ) ;
#72228=ADVANCED_FACE ( 'NONE', ( #69823 ), #46913, .F. ) ;
#72422=DIRECTION ( 'NONE',  ( -1.000000000000000000, -0.000000000000000000, -0.000000000000000000 ) ) ;
#72428=ORIENTED_EDGE ( 'NONE', *, *, #71716, .F. ) ;
#72524=DIRECTION ( 'NONE',  ( 1.000000000000000000, 0.000000000000000000, 0.000000000000000000 ) ) ;
#72555=CIRCLE ( 'NONE', #2962, 3.250000000000001332 ) ;
#72642=CIRCLE ( 'NONE', #40265, 0.2500000000000002220 ) ;
#73035=TOROIDAL_SURFACE ( 'NONE', #39474, 4.700000000000000178, 0.2999999999999999889 ) ;
#73140=EDGE_LOOP ( 'NONE', ( #63535, #60482, #67876, #46236, #55673 ) ) ;
#73167=ORIENTED_EDGE ( 'NONE', *, *, #31825, .T. ) ;
#73325=VERTEX_POINT ( 'NONE', #36933 ) ;
#73438=CARTESIAN_POINT ( 'NONE',  ( 26.00000000000000355, 3.334407072378456173E-16, -2.445500000000000007 ) ) ;
#73612=ORIENTED_EDGE ( 'NONE', *, *, #52036, .F. ) ;
#73857=ADVANCED_FACE ( 'NONE', ( #49873 ), #20193, .T. ) ;
#73876=SURFACE_STYLE_FILL_AREA ( #19777 ) ;
#73966=ORIENTED_EDGE ( 'NONE', *, *, #42982, .F. ) ;
#74002=DIRECTION ( 'NONE',  ( 0.000000000000000000, -0.5000000000000011102, -0.8660254037844380415 ) ) ;
#74178=DIRECTION ( 'NONE',  ( -1.000000000000000000, -0.000000000000000000, -0.000000000000000000 ) ) ;
#74225=EDGE_LOOP ( 'NONE', ( #67218, #38285, #2999 ) ) ;
#74244=ORIENTED_EDGE ( 'NONE', *, *, #57322, .F. ) ;
ENDSEC;
END-ISO-10303-21;
